ISO-10303-21;
HEADER;
/* Generated by software containing ST-Developer
 * from STEP Tools, Inc. (www.steptools.com) 
 */

FILE_DESCRIPTION(
/* description */ ('Union bypass pipe loop'),
/* implementation_level */ '2;1');

FILE_NAME(
/* name */ 'M5x70 body screw.step',
/* time_stamp */ '2026-10-27T21:00:29-07:00',
/* author */ (''),
/* organization */ (''),
/* preprocessor_version */ 'ST-DEVELOPER v20.2',
/* originating_system */ 'Autodesk Translation Framework v15.17.0.0',
/* authorisation */ '');

FILE_SCHEMA (('AUTOMOTIVE_DESIGN { 1 0 10303 214 3 1 1 }'));
ENDSEC;

DATA;
#10=MECHANICAL_DESIGN_GEOMETRIC_PRESENTATION_REPRESENTATION('',(#453),#10095);
#351=CONICAL_SURFACE('',#6109,0.4,0.785398163397448);
#352=CONICAL_SURFACE('',#6113,0.41,0.785398163397448);
#353=CONICAL_SURFACE('',#6117,0.26,0.463647609000806);
#372=ORIENTED_CLOSED_SHELL('',*,#5524,.F.);
#376=BREP_WITH_VOIDS('Body1',#5525,(#372));
#389=SHAPE_REPRESENTATION_RELATIONSHIP('SRR','None',#10258,#421);
#421=ADVANCED_BREP_SHAPE_REPRESENTATION('',(#376),#10070);
#453=STYLED_ITEM('',(#10507),#376);
#568=FACE_BOUND('',#1324,.T.);
#569=FACE_BOUND('',#1332,.T.);
#684=PLANE('',#6093);
#685=PLANE('',#6094);
#686=PLANE('',#6095);
#687=PLANE('',#6096);
#688=PLANE('',#6097);
#689=PLANE('',#6098);
#690=PLANE('',#6099);
#691=PLANE('',#6100);
#692=PLANE('',#6101);
#693=PLANE('',#6106);
#694=PLANE('',#6107);
#695=PLANE('',#6115);
#926=FACE_OUTER_BOUND('',#1315,.T.);
#927=FACE_OUTER_BOUND('',#1316,.T.);
#928=FACE_OUTER_BOUND('',#1317,.T.);
#929=FACE_OUTER_BOUND('',#1318,.T.);
#930=FACE_OUTER_BOUND('',#1319,.T.);
#931=FACE_OUTER_BOUND('',#1320,.T.);
#932=FACE_OUTER_BOUND('',#1321,.T.);
#933=FACE_OUTER_BOUND('',#1322,.T.);
#934=FACE_OUTER_BOUND('',#1323,.T.);
#935=FACE_OUTER_BOUND('',#1325,.T.);
#936=FACE_OUTER_BOUND('',#1326,.T.);
#937=FACE_OUTER_BOUND('',#1327,.T.);
#938=FACE_OUTER_BOUND('',#1328,.T.);
#939=FACE_OUTER_BOUND('',#1329,.T.);
#940=FACE_OUTER_BOUND('',#1330,.T.);
#941=FACE_OUTER_BOUND('',#1331,.T.);
#942=FACE_OUTER_BOUND('',#1333,.T.);
#943=FACE_OUTER_BOUND('',#1334,.T.);
#1315=EDGE_LOOP('',(#4126,#4127,#4128,#4129));
#1316=EDGE_LOOP('',(#4130,#4131,#4132,#4133));
#1317=EDGE_LOOP('',(#4134,#4135,#4136,#4137));
#1318=EDGE_LOOP('',(#4138,#4139,#4140,#4141));
#1319=EDGE_LOOP('',(#4142,#4143,#4144,#4145));
#1320=EDGE_LOOP('',(#4146,#4147,#4148,#4149));
#1321=EDGE_LOOP('',(#4150,#4151,#4152,#4153,#4154,#4155));
#1322=EDGE_LOOP('',(#4156,#4157,#4158,#4159,#4160,#4161));
#1323=EDGE_LOOP('',(#4162));
#1324=EDGE_LOOP('',(#4163));
#1325=EDGE_LOOP('',(#4164,#4165,#4166,#4167));
#1326=EDGE_LOOP('',(#4168));
#1327=EDGE_LOOP('',(#4169));
#1328=EDGE_LOOP('',(#4170,#4171,#4172,#4173));
#1329=EDGE_LOOP('',(#4174,#4175,#4176,#4177));
#1330=EDGE_LOOP('',(#4178,#4179,#4180,#4181));
#1331=EDGE_LOOP('',(#4182));
#1332=EDGE_LOOP('',(#4183));
#1333=EDGE_LOOP('',(#4184,#4185,#4186,#4187));
#1334=EDGE_LOOP('',(#4188,#4189,#4190,#4191));
#1732=LINE('',#8853,#2108);
#1733=LINE('',#8855,#2109);
#1734=LINE('',#8857,#2110);
#1735=LINE('',#8858,#2111);
#1736=LINE('',#8861,#2112);
#1737=LINE('',#8863,#2113);
#1738=LINE('',#8864,#2114);
#1739=LINE('',#8867,#2115);
#1740=LINE('',#8869,#2116);
#1741=LINE('',#8870,#2117);
#1742=LINE('',#8873,#2118);
#1743=LINE('',#8875,#2119);
#1744=LINE('',#8876,#2120);
#1745=LINE('',#8879,#2121);
#1746=LINE('',#8881,#2122);
#1747=LINE('',#8882,#2123);
#1748=LINE('',#8884,#2124);
#1749=LINE('',#8885,#2125);
#1750=LINE('',#8895,#2126);
#1751=LINE('',#8904,#2127);
#1752=LINE('',#8908,#2128);
#1753=LINE('',#8912,#2129);
#1754=LINE('',#8919,#2130);
#1755=LINE('',#8921,#2131);
#2108=VECTOR('',#7106,1.);
#2109=VECTOR('',#7107,1.);
#2110=VECTOR('',#7108,1.);
#2111=VECTOR('',#7109,1.);
#2112=VECTOR('',#7112,1.);
#2113=VECTOR('',#7113,1.);
#2114=VECTOR('',#7114,1.);
#2115=VECTOR('',#7117,1.);
#2116=VECTOR('',#7118,1.);
#2117=VECTOR('',#7119,1.);
#2118=VECTOR('',#7122,1.);
#2119=VECTOR('',#7123,1.);
#2120=VECTOR('',#7124,1.);
#2121=VECTOR('',#7127,1.);
#2122=VECTOR('',#7128,1.);
#2123=VECTOR('',#7129,1.);
#2124=VECTOR('',#7132,1.);
#2125=VECTOR('',#7133,1.);
#2126=VECTOR('',#7146,0.25);
#2127=VECTOR('',#7159,0.4);
#2128=VECTOR('',#7164,0.425);
#2129=VECTOR('',#7169,0.41);
#2130=VECTOR('',#7178,0.26);
#2131=VECTOR('',#7181,0.25);
#2460=CIRCLE('',#6102,0.25);
#2461=CIRCLE('',#6103,0.24505);
#2462=CIRCLE('',#6105,0.25);
#2463=CIRCLE('',#6108,0.375);
#2464=CIRCLE('',#6110,0.425);
#2465=CIRCLE('',#6112,0.425);
#2466=CIRCLE('',#6114,0.395);
#2467=CIRCLE('',#6116,0.27);
#2468=CIRCLE('',#6118,0.24505);
#2760=VERTEX_POINT('',#8851);
#2761=VERTEX_POINT('',#8852);
#2762=VERTEX_POINT('',#8854);
#2763=VERTEX_POINT('',#8856);
#2764=VERTEX_POINT('',#8860);
#2765=VERTEX_POINT('',#8862);
#2766=VERTEX_POINT('',#8866);
#2767=VERTEX_POINT('',#8868);
#2768=VERTEX_POINT('',#8872);
#2769=VERTEX_POINT('',#8874);
#2770=VERTEX_POINT('',#8878);
#2771=VERTEX_POINT('',#8880);
#2772=VERTEX_POINT('',#8889);
#2773=VERTEX_POINT('',#8891);
#2774=VERTEX_POINT('',#8894);
#2775=VERTEX_POINT('',#8899);
#2776=VERTEX_POINT('',#8902);
#2777=VERTEX_POINT('',#8906);
#2778=VERTEX_POINT('',#8910);
#2779=VERTEX_POINT('',#8914);
#2780=VERTEX_POINT('',#8917);
#3261=EDGE_CURVE('',#2760,#2761,#1732,.T.);
#3262=EDGE_CURVE('',#2761,#2762,#1733,.T.);
#3263=EDGE_CURVE('',#2762,#2763,#1734,.T.);
#3264=EDGE_CURVE('',#2760,#2763,#1735,.T.);
#3265=EDGE_CURVE('',#2761,#2764,#1736,.T.);
#3266=EDGE_CURVE('',#2764,#2765,#1737,.T.);
#3267=EDGE_CURVE('',#2765,#2762,#1738,.T.);
#3268=EDGE_CURVE('',#2764,#2766,#1739,.T.);
#3269=EDGE_CURVE('',#2766,#2767,#1740,.T.);
#3270=EDGE_CURVE('',#2767,#2765,#1741,.T.);
#3271=EDGE_CURVE('',#2766,#2768,#1742,.T.);
#3272=EDGE_CURVE('',#2768,#2769,#1743,.T.);
#3273=EDGE_CURVE('',#2769,#2767,#1744,.T.);
#3274=EDGE_CURVE('',#2768,#2770,#1745,.T.);
#3275=EDGE_CURVE('',#2770,#2771,#1746,.T.);
#3276=EDGE_CURVE('',#2771,#2769,#1747,.T.);
#3277=EDGE_CURVE('',#2770,#2760,#1748,.T.);
#3278=EDGE_CURVE('',#2763,#2771,#1749,.T.);
#3279=EDGE_CURVE('',#2772,#2772,#2460,.T.);
#3280=EDGE_CURVE('',#2773,#2773,#2461,.T.);
#3281=EDGE_CURVE('',#2772,#2774,#1750,.T.);
#3282=EDGE_CURVE('',#2774,#2774,#2462,.T.);
#3283=EDGE_CURVE('',#2775,#2775,#2463,.T.);
#3284=EDGE_CURVE('',#2776,#2776,#2464,.T.);
#3285=EDGE_CURVE('',#2776,#2775,#1751,.T.);
#3286=EDGE_CURVE('',#2777,#2777,#2465,.T.);
#3287=EDGE_CURVE('',#2777,#2776,#1752,.T.);
#3288=EDGE_CURVE('',#2778,#2778,#2466,.T.);
#3289=EDGE_CURVE('',#2778,#2777,#1753,.T.);
#3290=EDGE_CURVE('',#2779,#2779,#2467,.T.);
#3291=EDGE_CURVE('',#2780,#2780,#2468,.F.);
#3292=EDGE_CURVE('',#2780,#2779,#1754,.T.);
#3293=EDGE_CURVE('',#2773,#2780,#1755,.T.);
#4126=ORIENTED_EDGE('',*,*,#3261,.T.);
#4127=ORIENTED_EDGE('',*,*,#3262,.T.);
#4128=ORIENTED_EDGE('',*,*,#3263,.T.);
#4129=ORIENTED_EDGE('',*,*,#3264,.F.);
#4130=ORIENTED_EDGE('',*,*,#3265,.T.);
#4131=ORIENTED_EDGE('',*,*,#3266,.T.);
#4132=ORIENTED_EDGE('',*,*,#3267,.T.);
#4133=ORIENTED_EDGE('',*,*,#3262,.F.);
#4134=ORIENTED_EDGE('',*,*,#3268,.T.);
#4135=ORIENTED_EDGE('',*,*,#3269,.T.);
#4136=ORIENTED_EDGE('',*,*,#3270,.T.);
#4137=ORIENTED_EDGE('',*,*,#3266,.F.);
#4138=ORIENTED_EDGE('',*,*,#3271,.T.);
#4139=ORIENTED_EDGE('',*,*,#3272,.T.);
#4140=ORIENTED_EDGE('',*,*,#3273,.T.);
#4141=ORIENTED_EDGE('',*,*,#3269,.F.);
#4142=ORIENTED_EDGE('',*,*,#3274,.T.);
#4143=ORIENTED_EDGE('',*,*,#3275,.T.);
#4144=ORIENTED_EDGE('',*,*,#3276,.T.);
#4145=ORIENTED_EDGE('',*,*,#3272,.F.);
#4146=ORIENTED_EDGE('',*,*,#3277,.T.);
#4147=ORIENTED_EDGE('',*,*,#3264,.T.);
#4148=ORIENTED_EDGE('',*,*,#3278,.T.);
#4149=ORIENTED_EDGE('',*,*,#3275,.F.);
#4150=ORIENTED_EDGE('',*,*,#3277,.F.);
#4151=ORIENTED_EDGE('',*,*,#3274,.F.);
#4152=ORIENTED_EDGE('',*,*,#3271,.F.);
#4153=ORIENTED_EDGE('',*,*,#3268,.F.);
#4154=ORIENTED_EDGE('',*,*,#3265,.F.);
#4155=ORIENTED_EDGE('',*,*,#3261,.F.);
#4156=ORIENTED_EDGE('',*,*,#3278,.F.);
#4157=ORIENTED_EDGE('',*,*,#3263,.F.);
#4158=ORIENTED_EDGE('',*,*,#3267,.F.);
#4159=ORIENTED_EDGE('',*,*,#3270,.F.);
#4160=ORIENTED_EDGE('',*,*,#3273,.F.);
#4161=ORIENTED_EDGE('',*,*,#3276,.F.);
#4162=ORIENTED_EDGE('',*,*,#3279,.T.);
#4163=ORIENTED_EDGE('',*,*,#3280,.F.);
#4164=ORIENTED_EDGE('',*,*,#3279,.F.);
#4165=ORIENTED_EDGE('',*,*,#3281,.T.);
#4166=ORIENTED_EDGE('',*,*,#3282,.T.);
#4167=ORIENTED_EDGE('',*,*,#3281,.F.);
#4168=ORIENTED_EDGE('',*,*,#3282,.F.);
#4169=ORIENTED_EDGE('',*,*,#3283,.F.);
#4170=ORIENTED_EDGE('',*,*,#3284,.F.);
#4171=ORIENTED_EDGE('',*,*,#3285,.T.);
#4172=ORIENTED_EDGE('',*,*,#3283,.T.);
#4173=ORIENTED_EDGE('',*,*,#3285,.F.);
#4174=ORIENTED_EDGE('',*,*,#3286,.F.);
#4175=ORIENTED_EDGE('',*,*,#3287,.T.);
#4176=ORIENTED_EDGE('',*,*,#3284,.T.);
#4177=ORIENTED_EDGE('',*,*,#3287,.F.);
#4178=ORIENTED_EDGE('',*,*,#3288,.F.);
#4179=ORIENTED_EDGE('',*,*,#3289,.T.);
#4180=ORIENTED_EDGE('',*,*,#3286,.T.);
#4181=ORIENTED_EDGE('',*,*,#3289,.F.);
#4182=ORIENTED_EDGE('',*,*,#3288,.T.);
#4183=ORIENTED_EDGE('',*,*,#3290,.F.);
#4184=ORIENTED_EDGE('',*,*,#3291,.F.);
#4185=ORIENTED_EDGE('',*,*,#3292,.T.);
#4186=ORIENTED_EDGE('',*,*,#3290,.T.);
#4187=ORIENTED_EDGE('',*,*,#3292,.F.);
#4188=ORIENTED_EDGE('',*,*,#3280,.T.);
#4189=ORIENTED_EDGE('',*,*,#3293,.T.);
#4190=ORIENTED_EDGE('',*,*,#3291,.T.);
#4191=ORIENTED_EDGE('',*,*,#3293,.F.);
#5118=CYLINDRICAL_SURFACE('',#6104,0.25);
#5119=CYLINDRICAL_SURFACE('',#6111,0.425);
#5120=CYLINDRICAL_SURFACE('',#6119,0.24505);
#5275=ADVANCED_FACE('',(#926),#684,.F.);
#5276=ADVANCED_FACE('',(#927),#685,.F.);
#5277=ADVANCED_FACE('',(#928),#686,.F.);
#5278=ADVANCED_FACE('',(#929),#687,.F.);
#5279=ADVANCED_FACE('',(#930),#688,.F.);
#5280=ADVANCED_FACE('',(#931),#689,.F.);
#5281=ADVANCED_FACE('',(#932),#690,.F.);
#5282=ADVANCED_FACE('',(#933),#691,.F.);
#5283=ADVANCED_FACE('',(#934,#568),#692,.T.);
#5284=ADVANCED_FACE('',(#935),#5118,.T.);
#5285=ADVANCED_FACE('',(#936),#693,.F.);
#5286=ADVANCED_FACE('',(#937),#694,.T.);
#5287=ADVANCED_FACE('',(#938),#351,.T.);
#5288=ADVANCED_FACE('',(#939),#5119,.T.);
#5289=ADVANCED_FACE('',(#940),#352,.T.);
#5290=ADVANCED_FACE('',(#941,#569),#695,.T.);
#5291=ADVANCED_FACE('',(#942),#353,.T.);
#5292=ADVANCED_FACE('',(#943),#5120,.T.);
#5524=CLOSED_SHELL('',(#5275,#5276,#5277,#5278,#5279,#5280,#5281,#5282));
#5525=CLOSED_SHELL('',(#5283,#5284,#5285,#5286,#5287,#5288,#5289,#5290,
#5291,#5292));
#6092=AXIS2_PLACEMENT_3D('',#8849,#7102,#7103);
#6093=AXIS2_PLACEMENT_3D('',#8850,#7104,#7105);
#6094=AXIS2_PLACEMENT_3D('',#8859,#7110,#7111);
#6095=AXIS2_PLACEMENT_3D('',#8865,#7115,#7116);
#6096=AXIS2_PLACEMENT_3D('',#8871,#7120,#7121);
#6097=AXIS2_PLACEMENT_3D('',#8877,#7125,#7126);
#6098=AXIS2_PLACEMENT_3D('',#8883,#7130,#7131);
#6099=AXIS2_PLACEMENT_3D('',#8886,#7134,#7135);
#6100=AXIS2_PLACEMENT_3D('',#8887,#7136,#7137);
#6101=AXIS2_PLACEMENT_3D('',#8888,#7138,#7139);
#6102=AXIS2_PLACEMENT_3D('',#8890,#7140,#7141);
#6103=AXIS2_PLACEMENT_3D('',#8892,#7142,#7143);
#6104=AXIS2_PLACEMENT_3D('',#8893,#7144,#7145);
#6105=AXIS2_PLACEMENT_3D('',#8896,#7147,#7148);
#6106=AXIS2_PLACEMENT_3D('',#8897,#7149,#7150);
#6107=AXIS2_PLACEMENT_3D('',#8898,#7151,#7152);
#6108=AXIS2_PLACEMENT_3D('',#8900,#7153,#7154);
#6109=AXIS2_PLACEMENT_3D('',#8901,#7155,#7156);
#6110=AXIS2_PLACEMENT_3D('',#8903,#7157,#7158);
#6111=AXIS2_PLACEMENT_3D('',#8905,#7160,#7161);
#6112=AXIS2_PLACEMENT_3D('',#8907,#7162,#7163);
#6113=AXIS2_PLACEMENT_3D('',#8909,#7165,#7166);
#6114=AXIS2_PLACEMENT_3D('',#8911,#7167,#7168);
#6115=AXIS2_PLACEMENT_3D('',#8913,#7170,#7171);
#6116=AXIS2_PLACEMENT_3D('',#8915,#7172,#7173);
#6117=AXIS2_PLACEMENT_3D('',#8916,#7174,#7175);
#6118=AXIS2_PLACEMENT_3D('',#8918,#7176,#7177);
#6119=AXIS2_PLACEMENT_3D('',#8920,#7179,#7180);
#7102=DIRECTION('axis',(0.,0.,1.));
#7103=DIRECTION('refdir',(1.,0.,0.));
#7104=DIRECTION('center_axis',(0.866025403784439,0.,-0.5));
#7105=DIRECTION('ref_axis',(0.5,0.,0.866025403784439));
#7106=DIRECTION('',(-0.5,0.,-0.866025403784439));
#7107=DIRECTION('',(0.,-1.,0.));
#7108=DIRECTION('',(0.5,0.,0.866025403784439));
#7109=DIRECTION('',(0.,-1.,0.));
#7110=DIRECTION('center_axis',(1.20185167898973E-16,0.,-1.));
#7111=DIRECTION('ref_axis',(1.,0.,1.20185167898973E-16));
#7112=DIRECTION('',(-1.,0.,-1.20185167898973E-16));
#7113=DIRECTION('',(0.,-1.,0.));
#7114=DIRECTION('',(1.,0.,1.20185167898973E-16));
#7115=DIRECTION('center_axis',(-0.866025403784439,0.,-0.5));
#7116=DIRECTION('ref_axis',(0.5,0.,-0.866025403784439));
#7117=DIRECTION('',(-0.5,0.,0.866025403784439));
#7118=DIRECTION('',(0.,-1.,0.));
#7119=DIRECTION('',(0.5,0.,-0.866025403784439));
#7120=DIRECTION('center_axis',(-0.866025403784439,0.,0.5));
#7121=DIRECTION('ref_axis',(-0.5,0.,-0.866025403784439));
#7122=DIRECTION('',(0.5,0.,0.866025403784439));
#7123=DIRECTION('',(0.,-1.,0.));
#7124=DIRECTION('',(-0.5,0.,-0.866025403784439));
#7125=DIRECTION('center_axis',(-2.40370335797945E-16,0.,1.));
#7126=DIRECTION('ref_axis',(-1.,0.,-2.40370335797945E-16));
#7127=DIRECTION('',(1.,0.,2.40370335797945E-16));
#7128=DIRECTION('',(0.,-1.,0.));
#7129=DIRECTION('',(-1.,0.,-2.40370335797945E-16));
#7130=DIRECTION('center_axis',(0.866025403784439,0.,0.5));
#7131=DIRECTION('ref_axis',(-0.5,0.,0.866025403784439));
#7132=DIRECTION('',(0.5,0.,-0.866025403784439));
#7133=DIRECTION('',(-0.5,0.,0.866025403784439));
#7134=DIRECTION('center_axis',(0.,1.,0.));
#7135=DIRECTION('ref_axis',(1.,0.,0.));
#7136=DIRECTION('center_axis',(0.,-1.,0.));
#7137=DIRECTION('ref_axis',(0.,0.,-1.));
#7138=DIRECTION('center_axis',(0.,1.,0.));
#7139=DIRECTION('ref_axis',(1.,0.,0.));
#7140=DIRECTION('center_axis',(0.,1.,0.));
#7141=DIRECTION('ref_axis',(1.,0.,0.));
#7142=DIRECTION('center_axis',(0.,1.,0.));
#7143=DIRECTION('ref_axis',(1.,0.,0.));
#7144=DIRECTION('center_axis',(0.,1.,0.));
#7145=DIRECTION('ref_axis',(1.,0.,0.));
#7146=DIRECTION('',(0.,-1.,0.));
#7147=DIRECTION('center_axis',(0.,1.,0.));
#7148=DIRECTION('ref_axis',(1.,0.,0.));
#7149=DIRECTION('center_axis',(0.,1.,0.));
#7150=DIRECTION('ref_axis',(1.,0.,0.));
#7151=DIRECTION('center_axis',(0.,1.,0.));
#7152=DIRECTION('ref_axis',(0.,0.,1.));
#7153=DIRECTION('center_axis',(0.,-1.,0.));
#7154=DIRECTION('ref_axis',(1.,0.,0.));
#7155=DIRECTION('center_axis',(0.,-1.,0.));
#7156=DIRECTION('ref_axis',(1.,0.,0.));
#7157=DIRECTION('center_axis',(0.,-1.,0.));
#7158=DIRECTION('ref_axis',(1.,0.,0.));
#7159=DIRECTION('',(0.707106781186548,0.707106781186547,8.65956056235493E-17));
#7160=DIRECTION('center_axis',(0.,-1.,0.));
#7161=DIRECTION('ref_axis',(1.,0.,0.));
#7162=DIRECTION('center_axis',(0.,-1.,0.));
#7163=DIRECTION('ref_axis',(1.,0.,0.));
#7164=DIRECTION('',(0.,1.,0.));
#7165=DIRECTION('center_axis',(0.,1.,0.));
#7166=DIRECTION('ref_axis',(1.,0.,0.));
#7167=DIRECTION('center_axis',(0.,-1.,0.));
#7168=DIRECTION('ref_axis',(1.,0.,0.));
#7169=DIRECTION('',(-0.707106781186547,0.707106781186548,-8.65956056235493E-17));
#7170=DIRECTION('center_axis',(0.,-1.,0.));
#7171=DIRECTION('ref_axis',(0.,0.,-1.));
#7172=DIRECTION('center_axis',(0.,-1.,0.));
#7173=DIRECTION('ref_axis',(1.,0.,0.));
#7174=DIRECTION('center_axis',(0.,1.,0.));
#7175=DIRECTION('ref_axis',(1.,0.,0.));
#7176=DIRECTION('center_axis',(0.,1.,0.));
#7177=DIRECTION('ref_axis',(1.,0.,0.));
#7178=DIRECTION('',(-0.447213595499958,0.894427190999916,-5.47678698264203E-17));
#7179=DIRECTION('center_axis',(0.,-1.,0.));
#7180=DIRECTION('ref_axis',(1.,0.,0.));
#7181=DIRECTION('',(0.,1.,0.));
#8849=CARTESIAN_POINT('',(0.,0.,0.));
#8850=CARTESIAN_POINT('Origin',(0.115470053837925,-0.5,-0.2));
#8851=CARTESIAN_POINT('',(0.23094010767585,-0.5,0.));
#8852=CARTESIAN_POINT('',(0.115470053837925,-0.5,-0.2));
#8853=CARTESIAN_POINT('',(0.23094010767585,-0.5,0.));
#8854=CARTESIAN_POINT('',(0.115470053837925,-0.8,-0.2));
#8855=CARTESIAN_POINT('',(0.115470053837925,-0.5,-0.2));
#8856=CARTESIAN_POINT('',(0.23094010767585,-0.8,0.));
#8857=CARTESIAN_POINT('',(0.23094010767585,-0.8,0.));
#8858=CARTESIAN_POINT('',(0.23094010767585,-0.5,0.));
#8859=CARTESIAN_POINT('Origin',(-0.115470053837925,-0.5,-0.2));
#8860=CARTESIAN_POINT('',(-0.115470053837925,-0.5,-0.2));
#8861=CARTESIAN_POINT('',(0.115470053837925,-0.5,-0.2));
#8862=CARTESIAN_POINT('',(-0.115470053837925,-0.8,-0.2));
#8863=CARTESIAN_POINT('',(-0.115470053837925,-0.5,-0.2));
#8864=CARTESIAN_POINT('',(0.115470053837925,-0.8,-0.2));
#8865=CARTESIAN_POINT('Origin',(-0.23094010767585,-0.5,-2.77555756156289E-17));
#8866=CARTESIAN_POINT('',(-0.23094010767585,-0.5,-2.82820063659975E-17));
#8867=CARTESIAN_POINT('',(-0.115470053837925,-0.5,-0.2));
#8868=CARTESIAN_POINT('',(-0.23094010767585,-0.8,-2.77555756156289E-17));
#8869=CARTESIAN_POINT('',(-0.23094010767585,-0.5,-2.82820063659975E-17));
#8870=CARTESIAN_POINT('',(-0.115470053837925,-0.8,-0.2));
#8871=CARTESIAN_POINT('Origin',(-0.115470053837925,-0.5,0.2));
#8872=CARTESIAN_POINT('',(-0.115470053837925,-0.5,0.2));
#8873=CARTESIAN_POINT('',(-0.23094010767585,-0.5,-2.82820063659975E-17));
#8874=CARTESIAN_POINT('',(-0.115470053837925,-0.8,0.2));
#8875=CARTESIAN_POINT('',(-0.115470053837925,-0.5,0.2));
#8876=CARTESIAN_POINT('',(-0.23094010767585,-0.8,-2.82820063659975E-17));
#8877=CARTESIAN_POINT('Origin',(0.115470053837925,-0.5,0.2));
#8878=CARTESIAN_POINT('',(0.115470053837925,-0.5,0.2));
#8879=CARTESIAN_POINT('',(-0.115470053837925,-0.5,0.2));
#8880=CARTESIAN_POINT('',(0.115470053837925,-0.8,0.2));
#8881=CARTESIAN_POINT('',(0.115470053837925,-0.5,0.2));
#8882=CARTESIAN_POINT('',(-0.115470053837925,-0.8,0.2));
#8883=CARTESIAN_POINT('Origin',(0.23094010767585,-0.5,0.));
#8884=CARTESIAN_POINT('',(0.115470053837925,-0.5,0.2));
#8885=CARTESIAN_POINT('',(0.115470053837925,-0.8,0.2));
#8886=CARTESIAN_POINT('Origin',(0.,-0.5,0.));
#8887=CARTESIAN_POINT('Origin',(0.,-0.8,0.));
#8888=CARTESIAN_POINT('Origin',(0.,-1.9,0.));
#8889=CARTESIAN_POINT('',(-0.25,-1.9,3.06161699786838E-17));
#8890=CARTESIAN_POINT('Origin',(0.,-1.9,0.));
#8891=CARTESIAN_POINT('',(-0.24505,-1.9,3.00099698131059E-17));
#8892=CARTESIAN_POINT('Origin',(0.,-1.9,0.));
#8893=CARTESIAN_POINT('Origin',(0.,-7.,0.));
#8894=CARTESIAN_POINT('',(-0.25,-7.,3.06161699786838E-17));
#8895=CARTESIAN_POINT('',(-0.25,-7.,3.06161699786838E-17));
#8896=CARTESIAN_POINT('Origin',(0.,-7.,0.));
#8897=CARTESIAN_POINT('Origin',(0.,-7.,0.));
#8898=CARTESIAN_POINT('Origin',(0.375,0.5,0.));
#8899=CARTESIAN_POINT('',(-0.375,0.5,-4.59242549680257E-17));
#8900=CARTESIAN_POINT('Origin',(0.,0.5,0.));
#8901=CARTESIAN_POINT('Origin',(0.,0.475,0.));
#8902=CARTESIAN_POINT('',(-0.425,0.45,-5.20474889637625E-17));
#8903=CARTESIAN_POINT('Origin',(0.,0.45,0.));
#8904=CARTESIAN_POINT('',(-0.4,0.475,-4.89858719658941E-17));
#8905=CARTESIAN_POINT('Origin',(0.,0.24,0.));
#8906=CARTESIAN_POINT('',(-0.425,0.0299999999999998,-5.20474889637625E-17));
#8907=CARTESIAN_POINT('Origin',(0.,0.0299999999999998,0.));
#8908=CARTESIAN_POINT('',(-0.425,0.24,-5.20474889637625E-17));
#8909=CARTESIAN_POINT('Origin',(0.,0.0150000000000001,0.));
#8910=CARTESIAN_POINT('',(-0.395,4.85722573273506E-17,-4.83735485663204E-17));
#8911=CARTESIAN_POINT('Origin',(0.,0.,0.));
#8912=CARTESIAN_POINT('',(-0.41,0.0150000000000001,-5.02105187650415E-17));
#8913=CARTESIAN_POINT('Origin',(0.27,0.,0.));
#8914=CARTESIAN_POINT('',(-0.27,0.,-3.30654635769785E-17));
#8915=CARTESIAN_POINT('Origin',(0.,0.,0.));
#8916=CARTESIAN_POINT('Origin',(0.,-0.02,0.));
#8917=CARTESIAN_POINT('',(-0.24505,-0.0498999999999999,3.00099698131059E-17));
#8918=CARTESIAN_POINT('Origin',(0.,-0.0498999999999999,0.));
#8919=CARTESIAN_POINT('',(-0.26,-0.02,-3.18408167778312E-17));
#8920=CARTESIAN_POINT('Origin',(0.,-0.995,0.));
#8921=CARTESIAN_POINT('',(-0.24505,-0.995,-3.00099698131059E-17));
#10033=UNCERTAINTY_MEASURE_WITH_UNIT(LENGTH_MEASURE(0.001),#10096,
'DISTANCE_ACCURACY_VALUE',
'Maximum model space distance between geometric entities at asserted c
onnectivities');
#10058=UNCERTAINTY_MEASURE_WITH_UNIT(LENGTH_MEASURE(0.001),#10096,
'DISTANCE_ACCURACY_VALUE',
'Maximum model space distance between geometric entities at asserted c
onnectivities');
#10070=(
GEOMETRIC_REPRESENTATION_CONTEXT(3)
GLOBAL_UNCERTAINTY_ASSIGNED_CONTEXT((#10033))
GLOBAL_UNIT_ASSIGNED_CONTEXT((#10096,#10098,#10099))
REPRESENTATION_CONTEXT('','3D')
);
#10095=(
GEOMETRIC_REPRESENTATION_CONTEXT(3)
GLOBAL_UNCERTAINTY_ASSIGNED_CONTEXT((#10058))
GLOBAL_UNIT_ASSIGNED_CONTEXT((#10096,#10098,#10099))
REPRESENTATION_CONTEXT('','3D')
);
#10096=(
LENGTH_UNIT()
NAMED_UNIT(*)
SI_UNIT(.CENTI.,.METRE.)
);
#10098=(
NAMED_UNIT(*)
PLANE_ANGLE_UNIT()
SI_UNIT($,.RADIAN.)
);
#10099=(
NAMED_UNIT(*)
SI_UNIT($,.STERADIAN.)
SOLID_ANGLE_UNIT()
);
#10111=SHAPE_DEFINITION_REPRESENTATION(#10147,#10258);
#10147=PRODUCT_DEFINITION_SHAPE('',$,#10295);
#10258=SHAPE_REPRESENTATION('',(#6092),#10070);
#10283=PRODUCT_DEFINITION_CONTEXT('part definition',#10393,'design');
#10295=PRODUCT_DEFINITION('M5x70 body screw','M5x70 body screw',#10331,
#10283);
#10331=PRODUCT_DEFINITION_FORMATION('',$,#10406);
#10393=APPLICATION_CONTEXT(
'Core Data for Automotive Mechanical Design Process');
#10394=PRODUCT_CONTEXT('part definition',#10393,'mechanical');
#10406=PRODUCT('M5x70 body screw','M5x70 body screw','M5x70 body screw',
(#10394));
#10501=COLOUR_RGB('Black',0.12,0.14,0.17);
#10502=FILL_AREA_STYLE_COLOUR('',#10501);
#10503=FILL_AREA_STYLE('',(#10502));
#10504=SURFACE_STYLE_FILL_AREA(#10503);
#10505=SURFACE_SIDE_STYLE('',(#10504));
#10506=SURFACE_STYLE_USAGE(.BOTH.,#10505);
#10507=PRESENTATION_STYLE_ASSIGNMENT((#10506));
ENDSEC;
END-ISO-10303-21;
